ISO-10303-21;
HEADER;
/* Generated by software containing ST-Developer
 * from STEP Tools, Inc. (www.steptools.com) 
 */

FILE_DESCRIPTION(
/* description */ ('Bearing-mounted hook block'),
/* implementation_level */ '2;1');

FILE_NAME(
/* name */ 'Swivel thrust washer.step',
/* time_stamp */ '2026-10-28T22:30:11-07:00',
/* author */ (''),
/* organization */ (''),
/* preprocessor_version */ 'ST-DEVELOPER v20.2',
/* originating_system */ 'Autodesk Translation Framework v15.17.0.0',
/* authorisation */ '');

FILE_SCHEMA (('AUTOMOTIVE_DESIGN { 1 0 10303 214 3 1 1 }'));
ENDSEC;

DATA;
#10=MECHANICAL_DESIGN_GEOMETRIC_PRESENTATION_REPRESENTATION('',(#353),#7609);
#297=SHAPE_REPRESENTATION_RELATIONSHIP('SRR','None',#7747,#321);
#321=ADVANCED_BREP_SHAPE_REPRESENTATION('',(#382),#7607);
#353=STYLED_ITEM('',(#7938),#382);
#382=MANIFOLD_SOLID_BREP('Body1',#3952);
#593=LINE('',#7489,#823);
#594=LINE('',#7495,#824);
#823=VECTOR('',#5994,0.81);
#824=VECTOR('',#6001,1.5);
#918=CYLINDRICAL_SURFACE('',#4731,0.81);
#919=CYLINDRICAL_SURFACE('',#4734,1.5);
#997=FACE_BOUND('',#1539,.T.);
#998=FACE_BOUND('',#1541,.T.);
#1224=FACE_OUTER_BOUND('',#1536,.T.);
#1225=FACE_OUTER_BOUND('',#1537,.T.);
#1226=FACE_OUTER_BOUND('',#1538,.T.);
#1227=FACE_OUTER_BOUND('',#1540,.T.);
#1536=EDGE_LOOP('',(#3506,#3507,#3508,#3509));
#1537=EDGE_LOOP('',(#3510,#3511,#3512,#3513));
#1538=EDGE_LOOP('',(#3514));
#1539=EDGE_LOOP('',(#3515));
#1540=EDGE_LOOP('',(#3516));
#1541=EDGE_LOOP('',(#3517));
#1772=CIRCLE('',#4732,0.81);
#1773=CIRCLE('',#4733,0.81);
#1774=CIRCLE('',#4735,1.5);
#1775=CIRCLE('',#4736,1.5);
#2087=VERTEX_POINT('',#7486);
#2088=VERTEX_POINT('',#7488);
#2089=VERTEX_POINT('',#7492);
#2090=VERTEX_POINT('',#7494);
#2563=EDGE_CURVE('',#2087,#2087,#1772,.T.);
#2564=EDGE_CURVE('',#2087,#2088,#593,.T.);
#2565=EDGE_CURVE('',#2088,#2088,#1773,.T.);
#2566=EDGE_CURVE('',#2089,#2089,#1774,.T.);
#2567=EDGE_CURVE('',#2089,#2090,#594,.T.);
#2568=EDGE_CURVE('',#2090,#2090,#1775,.T.);
#3506=ORIENTED_EDGE('',*,*,#2563,.F.);
#3507=ORIENTED_EDGE('',*,*,#2564,.T.);
#3508=ORIENTED_EDGE('',*,*,#2565,.T.);
#3509=ORIENTED_EDGE('',*,*,#2564,.F.);
#3510=ORIENTED_EDGE('',*,*,#2566,.F.);
#3511=ORIENTED_EDGE('',*,*,#2567,.T.);
#3512=ORIENTED_EDGE('',*,*,#2568,.T.);
#3513=ORIENTED_EDGE('',*,*,#2567,.F.);
#3514=ORIENTED_EDGE('',*,*,#2566,.T.);
#3515=ORIENTED_EDGE('',*,*,#2563,.T.);
#3516=ORIENTED_EDGE('',*,*,#2568,.F.);
#3517=ORIENTED_EDGE('',*,*,#2565,.F.);
#3673=PLANE('',#4737);
#3674=PLANE('',#4738);
#3906=ADVANCED_FACE('',(#1224),#918,.F.);
#3907=ADVANCED_FACE('',(#1225),#919,.T.);
#3908=ADVANCED_FACE('',(#1226,#997),#3673,.T.);
#3909=ADVANCED_FACE('',(#1227,#998),#3674,.F.);
#3952=CLOSED_SHELL('',(#3906,#3907,#3908,#3909));
#4730=AXIS2_PLACEMENT_3D('',#7484,#5988,#5989);
#4731=AXIS2_PLACEMENT_3D('',#7485,#5990,#5991);
#4732=AXIS2_PLACEMENT_3D('',#7487,#5992,#5993);
#4733=AXIS2_PLACEMENT_3D('',#7490,#5995,#5996);
#4734=AXIS2_PLACEMENT_3D('',#7491,#5997,#5998);
#4735=AXIS2_PLACEMENT_3D('',#7493,#5999,#6000);
#4736=AXIS2_PLACEMENT_3D('',#7496,#6002,#6003);
#4737=AXIS2_PLACEMENT_3D('',#7497,#6004,#6005);
#4738=AXIS2_PLACEMENT_3D('',#7498,#6006,#6007);
#5988=DIRECTION('axis',(0.,0.,1.));
#5989=DIRECTION('refdir',(1.,0.,0.));
#5990=DIRECTION('center_axis',(0.,0.,1.));
#5991=DIRECTION('ref_axis',(1.,0.,0.));
#5992=DIRECTION('center_axis',(0.,0.,-1.));
#5993=DIRECTION('ref_axis',(1.,0.,0.));
#5994=DIRECTION('',(0.,0.,-1.));
#5995=DIRECTION('center_axis',(0.,0.,-1.));
#5996=DIRECTION('ref_axis',(1.,0.,0.));
#5997=DIRECTION('center_axis',(0.,0.,1.));
#5998=DIRECTION('ref_axis',(1.,0.,0.));
#5999=DIRECTION('center_axis',(0.,0.,1.));
#6000=DIRECTION('ref_axis',(1.,0.,0.));
#6001=DIRECTION('',(0.,0.,-1.));
#6002=DIRECTION('center_axis',(0.,0.,1.));
#6003=DIRECTION('ref_axis',(1.,0.,0.));
#6004=DIRECTION('center_axis',(0.,0.,1.));
#6005=DIRECTION('ref_axis',(1.,0.,0.));
#6006=DIRECTION('center_axis',(0.,0.,1.));
#6007=DIRECTION('ref_axis',(1.,0.,0.));
#7484=CARTESIAN_POINT('',(0.,0.,0.));
#7485=CARTESIAN_POINT('Origin',(0.,0.,5.5));
#7486=CARTESIAN_POINT('',(-0.81,-9.91963907309356E-17,5.7));
#7487=CARTESIAN_POINT('Origin',(0.,0.,5.7));
#7488=CARTESIAN_POINT('',(-0.81,-9.91963907309356E-17,5.5));
#7489=CARTESIAN_POINT('',(-0.81,-9.91963907309356E-17,5.5));
#7490=CARTESIAN_POINT('Origin',(0.,0.,5.5));
#7491=CARTESIAN_POINT('Origin',(0.,0.,5.5));
#7492=CARTESIAN_POINT('',(-1.5,-1.83697019872103E-16,5.7));
#7493=CARTESIAN_POINT('Origin',(0.,0.,5.7));
#7494=CARTESIAN_POINT('',(-1.5,-1.83697019872103E-16,5.5));
#7495=CARTESIAN_POINT('',(-1.5,-1.83697019872103E-16,5.5));
#7496=CARTESIAN_POINT('Origin',(0.,0.,5.5));
#7497=CARTESIAN_POINT('Origin',(0.,0.,5.7));
#7498=CARTESIAN_POINT('Origin',(0.,0.,5.5));
#7577=UNCERTAINTY_MEASURE_WITH_UNIT(LENGTH_MEASURE(0.001),#7610,
'DISTANCE_ACCURACY_VALUE',
'Maximum model space distance between geometric entities at asserted c
onnectivities');
#7579=UNCERTAINTY_MEASURE_WITH_UNIT(LENGTH_MEASURE(0.001),#7610,
'DISTANCE_ACCURACY_VALUE',
'Maximum model space distance between geometric entities at asserted c
onnectivities');
#7607=(
GEOMETRIC_REPRESENTATION_CONTEXT(3)
GLOBAL_UNCERTAINTY_ASSIGNED_CONTEXT((#7577))
GLOBAL_UNIT_ASSIGNED_CONTEXT((#7610,#7612,#7613))
REPRESENTATION_CONTEXT('','3D')
);
#7609=(
GEOMETRIC_REPRESENTATION_CONTEXT(3)
GLOBAL_UNCERTAINTY_ASSIGNED_CONTEXT((#7579))
GLOBAL_UNIT_ASSIGNED_CONTEXT((#7610,#7612,#7613))
REPRESENTATION_CONTEXT('','3D')
);
#7610=(
LENGTH_UNIT()
NAMED_UNIT(*)
SI_UNIT(.CENTI.,.METRE.)
);
#7612=(
NAMED_UNIT(*)
PLANE_ANGLE_UNIT()
SI_UNIT($,.RADIAN.)
);
#7613=(
NAMED_UNIT(*)
SI_UNIT($,.STERADIAN.)
SOLID_ANGLE_UNIT()
);
#7641=SHAPE_DEFINITION_REPRESENTATION(#7712,#7747);
#7712=PRODUCT_DEFINITION_SHAPE('',$,#7777);
#7747=SHAPE_REPRESENTATION('',(#4730),#7607);
#7749=PRODUCT_DEFINITION_CONTEXT('part definition',#7838,'design');
#7777=PRODUCT_DEFINITION('Swivel thrust washer','Swivel thrust washer',
#7806,#7749);
#7806=PRODUCT_DEFINITION_FORMATION('',$,#7867);
#7838=APPLICATION_CONTEXT(
'Core Data for Automotive Mechanical Design Process');
#7839=PRODUCT_CONTEXT('part definition',#7838,'mechanical');
#7867=PRODUCT('Swivel thrust washer','Swivel thrust washer',
'Swivel thrust washer',(#7839));
#7932=COLOUR_RGB('Black',0.12,0.14,0.17);
#7933=FILL_AREA_STYLE_COLOUR('',#7932);
#7934=FILL_AREA_STYLE('',(#7933));
#7935=SURFACE_STYLE_FILL_AREA(#7934);
#7936=SURFACE_SIDE_STYLE('',(#7935));
#7937=SURFACE_STYLE_USAGE(.BOTH.,#7936);
#7938=PRESENTATION_STYLE_ASSIGNMENT((#7937));
ENDSEC;
END-ISO-10303-21;
